ISO-10303-21;
HEADER;
/* Generated by software containing ST-Developer
 * from STEP Tools, Inc. (www.steptools.com) 
 */

FILE_DESCRIPTION(
/* description */ ('Bin tilter linkage'),
/* implementation_level */ '2;1');

FILE_NAME(
/* name */ 'M4 short cap screw (8).step',
/* time_stamp */ '2026-10-28T03:26:24-07:00',
/* author */ (''),
/* organization */ (''),
/* preprocessor_version */ 'ST-DEVELOPER v20.2',
/* originating_system */ 'Autodesk Translation Framework v15.17.0.0',
/* authorisation */ '');

FILE_SCHEMA (('AUTOMOTIVE_DESIGN { 1 0 10303 214 3 1 1 }'));
ENDSEC;

DATA;
#10=MECHANICAL_DESIGN_GEOMETRIC_PRESENTATION_REPRESENTATION('',(#904),#23728);
#692=SHAPE_REPRESENTATION_RELATIONSHIP('SRR','None',#24157,#798);
#798=ADVANCED_BREP_SHAPE_REPRESENTATION('',(#1017),#23657);
#904=STYLED_ITEM('',(#24772),#1017);
#1017=MANIFOLD_SOLID_BREP('Body1',#12435);
#1292=FACE_BOUND('',#3202,.T.);
#1651=PLANE('',#14387);
#1652=PLANE('',#14392);
#1653=PLANE('',#14395);
#2219=FACE_OUTER_BOUND('',#3201,.T.);
#2220=FACE_OUTER_BOUND('',#3203,.T.);
#2221=FACE_OUTER_BOUND('',#3204,.T.);
#2222=FACE_OUTER_BOUND('',#3205,.T.);
#2223=FACE_OUTER_BOUND('',#3206,.T.);
#3201=EDGE_LOOP('',(#9661));
#3202=EDGE_LOOP('',(#9662));
#3203=EDGE_LOOP('',(#9663,#9664,#9665,#9666));
#3204=EDGE_LOOP('',(#9667));
#3205=EDGE_LOOP('',(#9668,#9669,#9670,#9671));
#3206=EDGE_LOOP('',(#9672));
#4157=LINE('',#21199,#4832);
#4158=LINE('',#21205,#4833);
#4832=VECTOR('',#17212,0.35);
#4833=VECTOR('',#17221,0.199999999999999);
#5535=CIRCLE('',#14388,0.35);
#5536=CIRCLE('',#14389,0.199999999999999);
#5537=CIRCLE('',#14391,0.35);
#5538=CIRCLE('',#14394,0.199999999999999);
#6385=VERTEX_POINT('',#21193);
#6386=VERTEX_POINT('',#21195);
#6387=VERTEX_POINT('',#21198);
#6388=VERTEX_POINT('',#21203);
#7570=EDGE_CURVE('',#6385,#6385,#5535,.T.);
#7571=EDGE_CURVE('',#6386,#6386,#5536,.T.);
#7572=EDGE_CURVE('',#6385,#6387,#4157,.T.);
#7573=EDGE_CURVE('',#6387,#6387,#5537,.T.);
#7574=EDGE_CURVE('',#6388,#6388,#5538,.T.);
#7575=EDGE_CURVE('',#6388,#6386,#4158,.T.);
#9661=ORIENTED_EDGE('',*,*,#7570,.T.);
#9662=ORIENTED_EDGE('',*,*,#7571,.F.);
#9663=ORIENTED_EDGE('',*,*,#7570,.F.);
#9664=ORIENTED_EDGE('',*,*,#7572,.T.);
#9665=ORIENTED_EDGE('',*,*,#7573,.T.);
#9666=ORIENTED_EDGE('',*,*,#7572,.F.);
#9667=ORIENTED_EDGE('',*,*,#7573,.F.);
#9668=ORIENTED_EDGE('',*,*,#7574,.F.);
#9669=ORIENTED_EDGE('',*,*,#7575,.T.);
#9670=ORIENTED_EDGE('',*,*,#7571,.T.);
#9671=ORIENTED_EDGE('',*,*,#7575,.F.);
#9672=ORIENTED_EDGE('',*,*,#7574,.T.);
#11433=CYLINDRICAL_SURFACE('',#14390,0.35);
#11434=CYLINDRICAL_SURFACE('',#14393,0.199999999999999);
#11944=ADVANCED_FACE('',(#2219,#1292),#1651,.T.);
#11945=ADVANCED_FACE('',(#2220),#11433,.T.);
#11946=ADVANCED_FACE('',(#2221),#1652,.F.);
#11947=ADVANCED_FACE('',(#2222),#11434,.T.);
#11948=ADVANCED_FACE('',(#2223),#1653,.T.);
#12435=CLOSED_SHELL('',(#11944,#11945,#11946,#11947,#11948));
#14386=AXIS2_PLACEMENT_3D('',#21191,#17202,#17203);
#14387=AXIS2_PLACEMENT_3D('',#21192,#17204,#17205);
#14388=AXIS2_PLACEMENT_3D('',#21194,#17206,#17207);
#14389=AXIS2_PLACEMENT_3D('',#21196,#17208,#17209);
#14390=AXIS2_PLACEMENT_3D('',#21197,#17210,#17211);
#14391=AXIS2_PLACEMENT_3D('',#21200,#17213,#17214);
#14392=AXIS2_PLACEMENT_3D('',#21201,#17215,#17216);
#14393=AXIS2_PLACEMENT_3D('',#21202,#17217,#17218);
#14394=AXIS2_PLACEMENT_3D('',#21204,#17219,#17220);
#14395=AXIS2_PLACEMENT_3D('',#21206,#17222,#17223);
#17202=DIRECTION('axis',(0.,0.,1.));
#17203=DIRECTION('refdir',(1.,0.,0.));
#17204=DIRECTION('center_axis',(0.,1.,0.));
#17205=DIRECTION('ref_axis',(1.,0.,0.));
#17206=DIRECTION('center_axis',(0.,1.,0.));
#17207=DIRECTION('ref_axis',(1.,0.,0.));
#17208=DIRECTION('center_axis',(0.,1.,0.));
#17209=DIRECTION('ref_axis',(1.,0.,0.));
#17210=DIRECTION('center_axis',(0.,1.,0.));
#17211=DIRECTION('ref_axis',(1.,0.,0.));
#17212=DIRECTION('',(0.,-1.,0.));
#17213=DIRECTION('center_axis',(0.,1.,0.));
#17214=DIRECTION('ref_axis',(1.,0.,0.));
#17215=DIRECTION('center_axis',(0.,1.,0.));
#17216=DIRECTION('ref_axis',(1.,0.,0.));
#17217=DIRECTION('center_axis',(0.,1.,0.));
#17218=DIRECTION('ref_axis',(1.,0.,0.));
#17219=DIRECTION('center_axis',(0.,1.,0.));
#17220=DIRECTION('ref_axis',(1.,0.,0.));
#17221=DIRECTION('',(0.,-1.,0.));
#17222=DIRECTION('center_axis',(0.,1.,0.));
#17223=DIRECTION('ref_axis',(1.,0.,0.));
#21191=CARTESIAN_POINT('',(0.,0.,0.));
#21192=CARTESIAN_POINT('Origin',(10.7050737530542,-0.8,19.7283489784518));
#21193=CARTESIAN_POINT('',(10.3550737530542,-0.8,19.7283489784518));
#21194=CARTESIAN_POINT('Origin',(10.7050737530542,-0.8,19.7283489784518));
#21195=CARTESIAN_POINT('',(10.5050737530542,-0.8,19.7283489784518));
#21196=CARTESIAN_POINT('Origin',(10.7050737530542,-0.8,19.7283489784518));
#21197=CARTESIAN_POINT('Origin',(10.7050737530542,-1.2,19.7283489784518));
#21198=CARTESIAN_POINT('',(10.3550737530542,-1.2,19.7283489784518));
#21199=CARTESIAN_POINT('',(10.3550737530542,-1.2,19.7283489784518));
#21200=CARTESIAN_POINT('Origin',(10.7050737530542,-1.2,19.7283489784518));
#21201=CARTESIAN_POINT('Origin',(10.7050737530542,-1.2,19.7283489784518));
#21202=CARTESIAN_POINT('Origin',(10.7050737530542,-0.8,19.7283489784518));
#21203=CARTESIAN_POINT('',(10.5050737530542,-0.1,19.7283489784518));
#21204=CARTESIAN_POINT('Origin',(10.7050737530542,-0.1,19.7283489784518));
#21205=CARTESIAN_POINT('',(10.5050737530542,-0.8,19.7283489784518));
#21206=CARTESIAN_POINT('Origin',(10.7050737530542,-0.1,19.7283489784518));
#23540=UNCERTAINTY_MEASURE_WITH_UNIT(LENGTH_MEASURE(0.001),#23729,
'DISTANCE_ACCURACY_VALUE',
'Maximum model space distance between geometric entities at asserted c
onnectivities');
#23611=UNCERTAINTY_MEASURE_WITH_UNIT(LENGTH_MEASURE(0.001),#23729,
'DISTANCE_ACCURACY_VALUE',
'Maximum model space distance between geometric entities at asserted c
onnectivities');
#23657=(
GEOMETRIC_REPRESENTATION_CONTEXT(3)
GLOBAL_UNCERTAINTY_ASSIGNED_CONTEXT((#23540))
GLOBAL_UNIT_ASSIGNED_CONTEXT((#23729,#23731,#23732))
REPRESENTATION_CONTEXT('','3D')
);
#23728=(
GEOMETRIC_REPRESENTATION_CONTEXT(3)
GLOBAL_UNCERTAINTY_ASSIGNED_CONTEXT((#23611))
GLOBAL_UNIT_ASSIGNED_CONTEXT((#23729,#23731,#23732))
REPRESENTATION_CONTEXT('','3D')
);
#23729=(
LENGTH_UNIT()
NAMED_UNIT(*)
SI_UNIT(.CENTI.,.METRE.)
);
#23731=(
NAMED_UNIT(*)
PLANE_ANGLE_UNIT()
SI_UNIT($,.RADIAN.)
);
#23732=(
NAMED_UNIT(*)
SI_UNIT($,.STERADIAN.)
SOLID_ANGLE_UNIT()
);
#23778=SHAPE_DEFINITION_REPRESENTATION(#23894,#24157);
#23894=PRODUCT_DEFINITION_SHAPE('',$,#24274);
#24157=SHAPE_REPRESENTATION('',(#14386),#23657);
#24228=PRODUCT_DEFINITION_CONTEXT('part definition',#24578,'design');
#24274=PRODUCT_DEFINITION('M4 short cap screw (8)',
'M4 short cap screw (8)',#24390,#24228);
#24390=PRODUCT_DEFINITION_FORMATION('',$,#24625);
#24578=APPLICATION_CONTEXT(
'Core Data for Automotive Mechanical Design Process');
#24579=PRODUCT_CONTEXT('part definition',#24578,'mechanical');
#24625=PRODUCT('M4 short cap screw (8)','M4 short cap screw (8)',
'M4 short cap screw (8)',(#24579));
#24766=COLOUR_RGB('Black',0.12,0.14,0.17);
#24767=FILL_AREA_STYLE_COLOUR('',#24766);
#24768=FILL_AREA_STYLE('',(#24767));
#24769=SURFACE_STYLE_FILL_AREA(#24768);
#24770=SURFACE_SIDE_STYLE('',(#24769));
#24771=SURFACE_STYLE_USAGE(.BOTH.,#24770);
#24772=PRESENTATION_STYLE_ASSIGNMENT((#24771));
ENDSEC;
END-ISO-10303-21;
